ISO-10303-21;
HEADER;
/* Generated by software containing ST-Developer
 * from STEP Tools, Inc. (www.steptools.com) 
 */

FILE_DESCRIPTION(
/* description */ ('Drill jig with bushing plate'),
/* implementation_level */ '2;1');

FILE_NAME(
/* name */ 'Bonded foot (2).step',
/* time_stamp */ '2026-10-27T10:51:08-07:00',
/* author */ (''),
/* organization */ (''),
/* preprocessor_version */ 'ST-DEVELOPER v20.2',
/* originating_system */ 'Autodesk Translation Framework v15.17.0.0',
/* authorisation */ '');

FILE_SCHEMA (('AUTOMOTIVE_DESIGN { 1 0 10303 214 3 1 1 }'));
ENDSEC;

DATA;
#10=MECHANICAL_DESIGN_GEOMETRIC_PRESENTATION_REPRESENTATION('',(#226),#6638);
#178=SHAPE_REPRESENTATION_RELATIONSHIP('SRR','None',#6742,#202);
#202=ADVANCED_BREP_SHAPE_REPRESENTATION('',(#250),#6615);
#226=STYLED_ITEM('',(#6957),#250);
#250=MANIFOLD_SOLID_BREP('Body1',#3593);
#380=PLANE('',#3948);
#381=PLANE('',#3949);
#527=FACE_OUTER_BOUND('',#769,.T.);
#528=FACE_OUTER_BOUND('',#770,.T.);
#529=FACE_OUTER_BOUND('',#771,.T.);
#769=EDGE_LOOP('',(#2557,#2558,#2559,#2560));
#770=EDGE_LOOP('',(#2561));
#771=EDGE_LOOP('',(#2562));
#1058=LINE('',#5622,#1319);
#1319=VECTOR('',#4489,0.800000000000001);
#1584=CIRCLE('',#3946,0.800000000000001);
#1585=CIRCLE('',#3947,0.800000000000001);
#1760=VERTEX_POINT('',#5619);
#1761=VERTEX_POINT('',#5621);
#2066=EDGE_CURVE('',#1760,#1760,#1584,.T.);
#2067=EDGE_CURVE('',#1760,#1761,#1058,.T.);
#2068=EDGE_CURVE('',#1761,#1761,#1585,.T.);
#2557=ORIENTED_EDGE('',*,*,#2066,.F.);
#2558=ORIENTED_EDGE('',*,*,#2067,.T.);
#2559=ORIENTED_EDGE('',*,*,#2068,.T.);
#2560=ORIENTED_EDGE('',*,*,#2067,.F.);
#2561=ORIENTED_EDGE('',*,*,#2066,.T.);
#2562=ORIENTED_EDGE('',*,*,#2068,.F.);
#3315=CYLINDRICAL_SURFACE('',#3945,0.800000000000001);
#3402=ADVANCED_FACE('',(#527),#3315,.T.);
#3403=ADVANCED_FACE('',(#528),#380,.T.);
#3404=ADVANCED_FACE('',(#529),#381,.F.);
#3593=CLOSED_SHELL('',(#3402,#3403,#3404));
#3944=AXIS2_PLACEMENT_3D('',#5617,#4483,#4484);
#3945=AXIS2_PLACEMENT_3D('',#5618,#4485,#4486);
#3946=AXIS2_PLACEMENT_3D('',#5620,#4487,#4488);
#3947=AXIS2_PLACEMENT_3D('',#5623,#4490,#4491);
#3948=AXIS2_PLACEMENT_3D('',#5624,#4492,#4493);
#3949=AXIS2_PLACEMENT_3D('',#5625,#4494,#4495);
#4483=DIRECTION('axis',(0.,0.,1.));
#4484=DIRECTION('refdir',(1.,0.,0.));
#4485=DIRECTION('center_axis',(0.,0.,1.));
#4486=DIRECTION('ref_axis',(1.,0.,0.));
#4487=DIRECTION('center_axis',(0.,0.,1.));
#4488=DIRECTION('ref_axis',(1.,0.,0.));
#4489=DIRECTION('',(0.,0.,-1.));
#4490=DIRECTION('center_axis',(0.,0.,1.));
#4491=DIRECTION('ref_axis',(1.,0.,0.));
#4492=DIRECTION('center_axis',(0.,0.,1.));
#4493=DIRECTION('ref_axis',(1.,0.,0.));
#4494=DIRECTION('center_axis',(0.,0.,1.));
#4495=DIRECTION('ref_axis',(1.,0.,0.));
#5617=CARTESIAN_POINT('',(0.,0.,0.));
#5618=CARTESIAN_POINT('Origin',(11.,-7.,-0.5));
#5619=CARTESIAN_POINT('',(10.2,-7.,0.));
#5620=CARTESIAN_POINT('Origin',(11.,-7.,0.));
#5621=CARTESIAN_POINT('',(10.2,-7.,-0.5));
#5622=CARTESIAN_POINT('',(10.2,-7.,-0.5));
#5623=CARTESIAN_POINT('Origin',(11.,-7.,-0.5));
#5624=CARTESIAN_POINT('Origin',(11.,-7.,0.));
#5625=CARTESIAN_POINT('Origin',(11.,-7.,-0.5));
#6586=UNCERTAINTY_MEASURE_WITH_UNIT(LENGTH_MEASURE(0.001),#6639,
'DISTANCE_ACCURACY_VALUE',
'Maximum model space distance between geometric entities at asserted c
onnectivities');
#6609=UNCERTAINTY_MEASURE_WITH_UNIT(LENGTH_MEASURE(0.001),#6639,
'DISTANCE_ACCURACY_VALUE',
'Maximum model space distance between geometric entities at asserted c
onnectivities');
#6615=(
GEOMETRIC_REPRESENTATION_CONTEXT(3)
GLOBAL_UNCERTAINTY_ASSIGNED_CONTEXT((#6586))
GLOBAL_UNIT_ASSIGNED_CONTEXT((#6639,#6641,#6642))
REPRESENTATION_CONTEXT('','3D')
);
#6638=(
GEOMETRIC_REPRESENTATION_CONTEXT(3)
GLOBAL_UNCERTAINTY_ASSIGNED_CONTEXT((#6609))
GLOBAL_UNIT_ASSIGNED_CONTEXT((#6639,#6641,#6642))
REPRESENTATION_CONTEXT('','3D')
);
#6639=(
LENGTH_UNIT()
NAMED_UNIT(*)
SI_UNIT(.CENTI.,.METRE.)
);
#6641=(
NAMED_UNIT(*)
PLANE_ANGLE_UNIT()
SI_UNIT($,.RADIAN.)
);
#6642=(
NAMED_UNIT(*)
SI_UNIT($,.STERADIAN.)
SOLID_ANGLE_UNIT()
);
#6648=SHAPE_DEFINITION_REPRESENTATION(#6676,#6742);
#6676=PRODUCT_DEFINITION_SHAPE('',$,#6771);
#6742=SHAPE_REPRESENTATION('',(#3944),#6615);
#6765=PRODUCT_DEFINITION_CONTEXT('part definition',#6851,'design');
#6771=PRODUCT_DEFINITION('Bonded foot (2)','Bonded foot (2)',#6799,#6765);
#6799=PRODUCT_DEFINITION_FORMATION('',$,#6858);
#6851=APPLICATION_CONTEXT(
'Core Data for Automotive Mechanical Design Process');
#6852=PRODUCT_CONTEXT('part definition',#6851,'mechanical');
#6858=PRODUCT('Bonded foot (2)','Bonded foot (2)','Bonded foot (2)',(#6852));
#6951=COLOUR_RGB('Off White',0.89,0.88,0.83);
#6952=FILL_AREA_STYLE_COLOUR('',#6951);
#6953=FILL_AREA_STYLE('',(#6952));
#6954=SURFACE_STYLE_FILL_AREA(#6953);
#6955=SURFACE_SIDE_STYLE('',(#6954));
#6956=SURFACE_STYLE_USAGE(.BOTH.,#6955);
#6957=PRESENTATION_STYLE_ASSIGNMENT((#6956));
ENDSEC;
END-ISO-10303-21;
